ISO-10303-21;
HEADER;
/* Generated by software containing ST-Developer
 * from STEP Tools, Inc. (www.steptools.com) 
 */

FILE_DESCRIPTION(
/* description */ ('Double-row support with tensioned shaft'),
/* implementation_level */ '2;1');

FILE_NAME(
/* name */ 'Flange hole reducer (6).step',
/* time_stamp */ '2026-10-27T10:50:35-07:00',
/* author */ (''),
/* organization */ (''),
/* preprocessor_version */ 'ST-DEVELOPER v20.2',
/* originating_system */ 'Autodesk Translation Framework v15.17.0.0',
/* authorisation */ '');

FILE_SCHEMA (('AUTOMOTIVE_DESIGN { 1 0 10303 214 3 1 1 }'));
ENDSEC;

DATA;
#10=MECHANICAL_DESIGN_GEOMETRIC_PRESENTATION_REPRESENTATION('',(#492),#11559);
#428=SHAPE_REPRESENTATION_RELATIONSHIP('SRR','None',#11736,#460);
#460=ADVANCED_BREP_SHAPE_REPRESENTATION('',(#525),#11538);
#492=STYLED_ITEM('',(#11981),#525);
#525=MANIFOLD_SOLID_BREP('Body1',#6337);
#606=FACE_BOUND('',#1424,.T.);
#607=FACE_BOUND('',#1426,.T.);
#737=PLANE('',#6907);
#738=PLANE('',#6908);
#1013=FACE_OUTER_BOUND('',#1421,.T.);
#1014=FACE_OUTER_BOUND('',#1422,.T.);
#1015=FACE_OUTER_BOUND('',#1423,.T.);
#1016=FACE_OUTER_BOUND('',#1425,.T.);
#1421=EDGE_LOOP('',(#4750,#4751,#4752,#4753));
#1422=EDGE_LOOP('',(#4754,#4755,#4756,#4757));
#1423=EDGE_LOOP('',(#4758));
#1424=EDGE_LOOP('',(#4759));
#1425=EDGE_LOOP('',(#4760));
#1426=EDGE_LOOP('',(#4761));
#1876=LINE('',#9700,#2423);
#1877=LINE('',#9706,#2424);
#2423=VECTOR('',#7885,0.425);
#2424=VECTOR('',#7892,0.595);
#2912=CIRCLE('',#6902,0.425);
#2913=CIRCLE('',#6903,0.425);
#2914=CIRCLE('',#6905,0.595);
#2915=CIRCLE('',#6906,0.595);
#3167=VERTEX_POINT('',#9697);
#3168=VERTEX_POINT('',#9699);
#3169=VERTEX_POINT('',#9703);
#3170=VERTEX_POINT('',#9705);
#3760=EDGE_CURVE('',#3167,#3167,#2912,.T.);
#3761=EDGE_CURVE('',#3167,#3168,#1876,.T.);
#3762=EDGE_CURVE('',#3168,#3168,#2913,.T.);
#3763=EDGE_CURVE('',#3169,#3169,#2914,.T.);
#3764=EDGE_CURVE('',#3169,#3170,#1877,.T.);
#3765=EDGE_CURVE('',#3170,#3170,#2915,.T.);
#4750=ORIENTED_EDGE('',*,*,#3760,.F.);
#4751=ORIENTED_EDGE('',*,*,#3761,.T.);
#4752=ORIENTED_EDGE('',*,*,#3762,.T.);
#4753=ORIENTED_EDGE('',*,*,#3761,.F.);
#4754=ORIENTED_EDGE('',*,*,#3763,.F.);
#4755=ORIENTED_EDGE('',*,*,#3764,.T.);
#4756=ORIENTED_EDGE('',*,*,#3765,.T.);
#4757=ORIENTED_EDGE('',*,*,#3764,.F.);
#4758=ORIENTED_EDGE('',*,*,#3763,.T.);
#4759=ORIENTED_EDGE('',*,*,#3760,.T.);
#4760=ORIENTED_EDGE('',*,*,#3765,.F.);
#4761=ORIENTED_EDGE('',*,*,#3762,.F.);
#5928=CYLINDRICAL_SURFACE('',#6901,0.425);
#5929=CYLINDRICAL_SURFACE('',#6904,0.595);
#6076=ADVANCED_FACE('',(#1013),#5928,.F.);
#6077=ADVANCED_FACE('',(#1014),#5929,.T.);
#6078=ADVANCED_FACE('',(#1015,#606),#737,.T.);
#6079=ADVANCED_FACE('',(#1016,#607),#738,.F.);
#6337=CLOSED_SHELL('',(#6076,#6077,#6078,#6079));
#6900=AXIS2_PLACEMENT_3D('',#9695,#7879,#7880);
#6901=AXIS2_PLACEMENT_3D('',#9696,#7881,#7882);
#6902=AXIS2_PLACEMENT_3D('',#9698,#7883,#7884);
#6903=AXIS2_PLACEMENT_3D('',#9701,#7886,#7887);
#6904=AXIS2_PLACEMENT_3D('',#9702,#7888,#7889);
#6905=AXIS2_PLACEMENT_3D('',#9704,#7890,#7891);
#6906=AXIS2_PLACEMENT_3D('',#9707,#7893,#7894);
#6907=AXIS2_PLACEMENT_3D('',#9708,#7895,#7896);
#6908=AXIS2_PLACEMENT_3D('',#9709,#7897,#7898);
#7879=DIRECTION('axis',(0.,0.,1.));
#7880=DIRECTION('refdir',(1.,0.,0.));
#7881=DIRECTION('center_axis',(0.,1.,0.));
#7882=DIRECTION('ref_axis',(1.,0.,0.));
#7883=DIRECTION('center_axis',(0.,-1.,0.));
#7884=DIRECTION('ref_axis',(1.,0.,0.));
#7885=DIRECTION('',(0.,-1.,0.));
#7886=DIRECTION('center_axis',(0.,-1.,0.));
#7887=DIRECTION('ref_axis',(1.,0.,0.));
#7888=DIRECTION('center_axis',(0.,1.,0.));
#7889=DIRECTION('ref_axis',(1.,0.,0.));
#7890=DIRECTION('center_axis',(0.,1.,0.));
#7891=DIRECTION('ref_axis',(1.,0.,0.));
#7892=DIRECTION('',(0.,-1.,0.));
#7893=DIRECTION('center_axis',(0.,1.,0.));
#7894=DIRECTION('ref_axis',(1.,0.,0.));
#7895=DIRECTION('center_axis',(0.,1.,0.));
#7896=DIRECTION('ref_axis',(1.,0.,0.));
#7897=DIRECTION('center_axis',(0.,1.,0.));
#7898=DIRECTION('ref_axis',(1.,0.,0.));
#9695=CARTESIAN_POINT('',(0.,0.,0.));
#9696=CARTESIAN_POINT('Origin',(3.2,17.5,6.8));
#9697=CARTESIAN_POINT('',(2.775,18.5,6.8));
#9698=CARTESIAN_POINT('Origin',(3.2,18.5,6.8));
#9699=CARTESIAN_POINT('',(2.775,17.5,6.8));
#9700=CARTESIAN_POINT('',(2.775,17.5,6.8));
#9701=CARTESIAN_POINT('Origin',(3.2,17.5,6.8));
#9702=CARTESIAN_POINT('Origin',(3.2,17.5,6.8));
#9703=CARTESIAN_POINT('',(2.605,18.5,6.8));
#9704=CARTESIAN_POINT('Origin',(3.2,18.5,6.8));
#9705=CARTESIAN_POINT('',(2.605,17.5,6.8));
#9706=CARTESIAN_POINT('',(2.605,17.5,6.8));
#9707=CARTESIAN_POINT('Origin',(3.2,17.5,6.8));
#9708=CARTESIAN_POINT('Origin',(3.2,18.5,6.8));
#9709=CARTESIAN_POINT('Origin',(3.2,17.5,6.8));
#11501=UNCERTAINTY_MEASURE_WITH_UNIT(LENGTH_MEASURE(0.001),#11560,
'DISTANCE_ACCURACY_VALUE',
'Maximum model space distance between geometric entities at asserted c
onnectivities');
#11522=UNCERTAINTY_MEASURE_WITH_UNIT(LENGTH_MEASURE(0.001),#11560,
'DISTANCE_ACCURACY_VALUE',
'Maximum model space distance between geometric entities at asserted c
onnectivities');
#11538=(
GEOMETRIC_REPRESENTATION_CONTEXT(3)
GLOBAL_UNCERTAINTY_ASSIGNED_CONTEXT((#11501))
GLOBAL_UNIT_ASSIGNED_CONTEXT((#11560,#11562,#11563))
REPRESENTATION_CONTEXT('','3D')
);
#11559=(
GEOMETRIC_REPRESENTATION_CONTEXT(3)
GLOBAL_UNCERTAINTY_ASSIGNED_CONTEXT((#11522))
GLOBAL_UNIT_ASSIGNED_CONTEXT((#11560,#11562,#11563))
REPRESENTATION_CONTEXT('','3D')
);
#11560=(
LENGTH_UNIT()
NAMED_UNIT(*)
SI_UNIT(.CENTI.,.METRE.)
);
#11562=(
NAMED_UNIT(*)
PLANE_ANGLE_UNIT()
SI_UNIT($,.RADIAN.)
);
#11563=(
NAMED_UNIT(*)
SI_UNIT($,.STERADIAN.)
SOLID_ANGLE_UNIT()
);
#11579=SHAPE_DEFINITION_REPRESENTATION(#11615,#11736);
#11615=PRODUCT_DEFINITION_SHAPE('',$,#11773);
#11736=SHAPE_REPRESENTATION('',(#6900),#11538);
#11757=PRODUCT_DEFINITION_CONTEXT('part definition',#11867,'design');
#11773=PRODUCT_DEFINITION('Flange hole reducer (6)',
'Flange hole reducer (6)',#11809,#11757);
#11809=PRODUCT_DEFINITION_FORMATION('',$,#11884);
#11867=APPLICATION_CONTEXT(
'Core Data for Automotive Mechanical Design Process');
#11868=PRODUCT_CONTEXT('part definition',#11867,'mechanical');
#11884=PRODUCT('Flange hole reducer (6)','Flange hole reducer (6)',
'Flange hole reducer (6)',(#11868));
#11975=COLOUR_RGB('Off White',0.89,0.88,0.83);
#11976=FILL_AREA_STYLE_COLOUR('',#11975);
#11977=FILL_AREA_STYLE('',(#11976));
#11978=SURFACE_STYLE_FILL_AREA(#11977);
#11979=SURFACE_SIDE_STYLE('',(#11978));
#11980=SURFACE_STYLE_USAGE(.BOTH.,#11979);
#11981=PRESENTATION_STYLE_ASSIGNMENT((#11980));
ENDSEC;
END-ISO-10303-21;
